ISO-10303-21;
HEADER;
/* Generated by software containing ST-Developer
 * from STEP Tools, Inc. (www.steptools.com) 
 */

FILE_DESCRIPTION(
/* description */ ('Dual-rail gantry carriage'),
/* implementation_level */ '2;1');

FILE_NAME(
/* name */ 'Flat Washer - M4.step',
/* time_stamp */ '2026-10-27T10:49:15-07:00',
/* author */ (''),
/* organization */ (''),
/* preprocessor_version */ 'ST-DEVELOPER v20.2',
/* originating_system */ 'Autodesk Translation Framework v15.17.0.0',
/* authorisation */ '');

FILE_SCHEMA (('AUTOMOTIVE_DESIGN { 1 0 10303 214 3 1 1 }'));
ENDSEC;

DATA;
#10=MECHANICAL_DESIGN_GEOMETRIC_PRESENTATION_REPRESENTATION('',(#614),#12804);
#514=CONICAL_SURFACE('',#8406,0.225,0.785398163397448);
#552=SHAPE_REPRESENTATION_RELATIONSHIP('SRR','None',#13032,#583);
#583=ADVANCED_BREP_SHAPE_REPRESENTATION('',(#641),#12802);
#614=STYLED_ITEM('',(#13254),#641);
#641=MANIFOLD_SOLID_BREP('Body1',#7396);
#761=FACE_BOUND('',#1927,.T.);
#762=FACE_BOUND('',#1930,.T.);
#1035=PLANE('',#8411);
#1036=PLANE('',#8415);
#1416=FACE_OUTER_BOUND('',#1924,.T.);
#1417=FACE_OUTER_BOUND('',#1925,.T.);
#1418=FACE_OUTER_BOUND('',#1926,.T.);
#1419=FACE_OUTER_BOUND('',#1928,.T.);
#1420=FACE_OUTER_BOUND('',#1929,.T.);
#1924=EDGE_LOOP('',(#6813,#6814,#6815,#6816));
#1925=EDGE_LOOP('',(#6817,#6818,#6819,#6820));
#1926=EDGE_LOOP('',(#6821));
#1927=EDGE_LOOP('',(#6822));
#1928=EDGE_LOOP('',(#6823,#6824,#6825,#6826));
#1929=EDGE_LOOP('',(#6827));
#1930=EDGE_LOOP('',(#6828));
#2631=LINE('',#12606,#3340);
#2632=LINE('',#12610,#3341);
#2633=LINE('',#12617,#3342);
#3340=VECTOR('',#10504,0.225);
#3341=VECTOR('',#10509,0.215);
#3342=VECTOR('',#10518,0.45);
#3554=CIRCLE('',#8407,0.235);
#3555=CIRCLE('',#8408,0.215);
#3556=CIRCLE('',#8410,0.215);
#3557=CIRCLE('',#8412,0.45);
#3558=CIRCLE('',#8414,0.45);
#4132=VERTEX_POINT('',#12603);
#4133=VERTEX_POINT('',#12605);
#4134=VERTEX_POINT('',#12609);
#4135=VERTEX_POINT('',#12613);
#4136=VERTEX_POINT('',#12616);
#5029=EDGE_CURVE('',#4132,#4132,#3554,.T.);
#5030=EDGE_CURVE('',#4132,#4133,#2631,.T.);
#5031=EDGE_CURVE('',#4133,#4133,#3555,.T.);
#5032=EDGE_CURVE('',#4133,#4134,#2632,.T.);
#5033=EDGE_CURVE('',#4134,#4134,#3556,.T.);
#5034=EDGE_CURVE('',#4135,#4135,#3557,.T.);
#5035=EDGE_CURVE('',#4135,#4136,#2633,.T.);
#5036=EDGE_CURVE('',#4136,#4136,#3558,.T.);
#6813=ORIENTED_EDGE('',*,*,#5029,.T.);
#6814=ORIENTED_EDGE('',*,*,#5030,.T.);
#6815=ORIENTED_EDGE('',*,*,#5031,.T.);
#6816=ORIENTED_EDGE('',*,*,#5030,.F.);
#6817=ORIENTED_EDGE('',*,*,#5031,.F.);
#6818=ORIENTED_EDGE('',*,*,#5032,.T.);
#6819=ORIENTED_EDGE('',*,*,#5033,.T.);
#6820=ORIENTED_EDGE('',*,*,#5032,.F.);
#6821=ORIENTED_EDGE('',*,*,#5034,.T.);
#6822=ORIENTED_EDGE('',*,*,#5029,.F.);
#6823=ORIENTED_EDGE('',*,*,#5034,.F.);
#6824=ORIENTED_EDGE('',*,*,#5035,.T.);
#6825=ORIENTED_EDGE('',*,*,#5036,.T.);
#6826=ORIENTED_EDGE('',*,*,#5035,.F.);
#6827=ORIENTED_EDGE('',*,*,#5036,.F.);
#6828=ORIENTED_EDGE('',*,*,#5033,.F.);
#6970=CYLINDRICAL_SURFACE('',#8409,0.215);
#6971=CYLINDRICAL_SURFACE('',#8413,0.45);
#7342=ADVANCED_FACE('',(#1416),#514,.F.);
#7343=ADVANCED_FACE('',(#1417),#6970,.F.);
#7344=ADVANCED_FACE('',(#1418,#761),#1035,.T.);
#7345=ADVANCED_FACE('',(#1419),#6971,.T.);
#7346=ADVANCED_FACE('',(#1420,#762),#1036,.F.);
#7396=CLOSED_SHELL('',(#7342,#7343,#7344,#7345,#7346));
#8405=AXIS2_PLACEMENT_3D('',#12601,#10498,#10499);
#8406=AXIS2_PLACEMENT_3D('',#12602,#10500,#10501);
#8407=AXIS2_PLACEMENT_3D('',#12604,#10502,#10503);
#8408=AXIS2_PLACEMENT_3D('',#12607,#10505,#10506);
#8409=AXIS2_PLACEMENT_3D('',#12608,#10507,#10508);
#8410=AXIS2_PLACEMENT_3D('',#12611,#10510,#10511);
#8411=AXIS2_PLACEMENT_3D('',#12612,#10512,#10513);
#8412=AXIS2_PLACEMENT_3D('',#12614,#10514,#10515);
#8413=AXIS2_PLACEMENT_3D('',#12615,#10516,#10517);
#8414=AXIS2_PLACEMENT_3D('',#12618,#10519,#10520);
#8415=AXIS2_PLACEMENT_3D('',#12619,#10521,#10522);
#10498=DIRECTION('axis',(0.,0.,1.));
#10499=DIRECTION('refdir',(1.,0.,0.));
#10500=DIRECTION('center_axis',(0.,1.,0.));
#10501=DIRECTION('ref_axis',(1.,0.,0.));
#10502=DIRECTION('center_axis',(0.,1.,0.));
#10503=DIRECTION('ref_axis',(1.,0.,0.));
#10504=DIRECTION('',(0.707106781186547,-0.707106781186548,-8.65956056235493E-17));
#10505=DIRECTION('center_axis',(0.,-1.,0.));
#10506=DIRECTION('ref_axis',(1.,0.,0.));
#10507=DIRECTION('center_axis',(0.,1.,0.));
#10508=DIRECTION('ref_axis',(1.,0.,0.));
#10509=DIRECTION('',(0.,-1.,0.));
#10510=DIRECTION('center_axis',(0.,-1.,0.));
#10511=DIRECTION('ref_axis',(1.,0.,0.));
#10512=DIRECTION('center_axis',(0.,1.,0.));
#10513=DIRECTION('ref_axis',(1.,0.,0.));
#10514=DIRECTION('center_axis',(0.,1.,0.));
#10515=DIRECTION('ref_axis',(1.,0.,0.));
#10516=DIRECTION('center_axis',(0.,1.,0.));
#10517=DIRECTION('ref_axis',(1.,0.,0.));
#10518=DIRECTION('',(0.,-1.,0.));
#10519=DIRECTION('center_axis',(0.,1.,0.));
#10520=DIRECTION('ref_axis',(1.,0.,0.));
#10521=DIRECTION('center_axis',(0.,1.,0.));
#10522=DIRECTION('ref_axis',(1.,0.,0.));
#12601=CARTESIAN_POINT('',(0.,0.,0.));
#12602=CARTESIAN_POINT('Origin',(0.,0.07,0.));
#12603=CARTESIAN_POINT('',(-0.235,0.08,2.87791997799628E-17));
#12604=CARTESIAN_POINT('Origin',(0.,0.08,0.));
#12605=CARTESIAN_POINT('',(-0.215,0.06,-2.63299061816681E-17));
#12606=CARTESIAN_POINT('',(-0.225,0.07,2.75545529808154E-17));
#12607=CARTESIAN_POINT('Origin',(0.,0.06,0.));
#12608=CARTESIAN_POINT('Origin',(0.,0.,0.));
#12609=CARTESIAN_POINT('',(-0.215,0.,2.63299061816681E-17));
#12610=CARTESIAN_POINT('',(-0.215,0.,2.63299061816681E-17));
#12611=CARTESIAN_POINT('Origin',(0.,0.,0.));
#12612=CARTESIAN_POINT('Origin',(0.,0.08,0.));
#12613=CARTESIAN_POINT('',(-0.45,0.08,5.51091059616309E-17));
#12614=CARTESIAN_POINT('Origin',(0.,0.08,0.));
#12615=CARTESIAN_POINT('Origin',(0.,0.,0.));
#12616=CARTESIAN_POINT('',(-0.45,0.,5.51091059616309E-17));
#12617=CARTESIAN_POINT('',(-0.45,0.,5.51091059616309E-17));
#12618=CARTESIAN_POINT('Origin',(0.,0.,0.));
#12619=CARTESIAN_POINT('Origin',(0.,0.,0.));
#12766=UNCERTAINTY_MEASURE_WITH_UNIT(LENGTH_MEASURE(0.001),#12805,
'DISTANCE_ACCURACY_VALUE',
'Maximum model space distance between geometric entities at asserted c
onnectivities');
#12768=UNCERTAINTY_MEASURE_WITH_UNIT(LENGTH_MEASURE(0.001),#12805,
'DISTANCE_ACCURACY_VALUE',
'Maximum model space distance between geometric entities at asserted c
onnectivities');
#12802=(
GEOMETRIC_REPRESENTATION_CONTEXT(3)
GLOBAL_UNCERTAINTY_ASSIGNED_CONTEXT((#12766))
GLOBAL_UNIT_ASSIGNED_CONTEXT((#12805,#12807,#12808))
REPRESENTATION_CONTEXT('','3D')
);
#12804=(
GEOMETRIC_REPRESENTATION_CONTEXT(3)
GLOBAL_UNCERTAINTY_ASSIGNED_CONTEXT((#12768))
GLOBAL_UNIT_ASSIGNED_CONTEXT((#12805,#12807,#12808))
REPRESENTATION_CONTEXT('','3D')
);
#12805=(
LENGTH_UNIT()
NAMED_UNIT(*)
SI_UNIT(.CENTI.,.METRE.)
);
#12807=(
NAMED_UNIT(*)
PLANE_ANGLE_UNIT()
SI_UNIT($,.RADIAN.)
);
#12808=(
NAMED_UNIT(*)
SI_UNIT($,.STERADIAN.)
SOLID_ANGLE_UNIT()
);
#12842=SHAPE_DEFINITION_REPRESENTATION(#12950,#13032);
#12950=PRODUCT_DEFINITION_SHAPE('',$,#13068);
#13032=SHAPE_REPRESENTATION('',(#8405),#12802);
#13034=PRODUCT_DEFINITION_CONTEXT('part definition',#13141,'design');
#13068=PRODUCT_DEFINITION('Flat Washer - M4','Flat Washer - M4',#13103,
#13034);
#13103=PRODUCT_DEFINITION_FORMATION('',$,#13176);
#13141=APPLICATION_CONTEXT(
'Core Data for Automotive Mechanical Design Process');
#13142=PRODUCT_CONTEXT('part definition',#13141,'mechanical');
#13176=PRODUCT('Flat Washer - M4','Flat Washer - M4','Flat Washer - M4',
(#13142));
#13248=COLOUR_RGB('Black',0.12,0.14,0.17);
#13249=FILL_AREA_STYLE_COLOUR('',#13248);
#13250=FILL_AREA_STYLE('',(#13249));
#13251=SURFACE_STYLE_FILL_AREA(#13250);
#13252=SURFACE_SIDE_STYLE('',(#13251));
#13253=SURFACE_STYLE_USAGE(.BOTH.,#13252);
#13254=PRESENTATION_STYLE_ASSIGNMENT((#13253));
ENDSEC;
END-ISO-10303-21;
